ISO-10303-21;
HEADER;
/* Generated by software containing ST-Developer
 * from STEP Tools, Inc. (www.steptools.com) 
 */

FILE_DESCRIPTION(
/* description */ ('Shaft runout checking stand'),
/* implementation_level */ '2;1');

FILE_NAME(
/* name */ 'Inner race spacer (1).step',
/* time_stamp */ '2026-11-02T21:12:33-08:00',
/* author */ (''),
/* organization */ (''),
/* preprocessor_version */ 'ST-DEVELOPER v20.2',
/* originating_system */ 'Autodesk Translation Framework v15.17.0.0',
/* authorisation */ '');

FILE_SCHEMA (('AUTOMOTIVE_DESIGN { 1 0 10303 214 3 1 1 }'));
ENDSEC;

DATA;
#10=MECHANICAL_DESIGN_GEOMETRIC_PRESENTATION_REPRESENTATION('',(#472),#11748);
#386=SHAPE_REPRESENTATION_RELATIONSHIP('SRR','None',#11935,#429);
#429=ADVANCED_BREP_SHAPE_REPRESENTATION('',(#523),#11711);
#472=STYLED_ITEM('',(#12170),#523);
#523=MANIFOLD_SOLID_BREP('Body1',#6215);
#603=FACE_BOUND('',#1571,.T.);
#604=FACE_BOUND('',#1573,.T.);
#728=CIRCLE('',#6925,0.505);
#729=CIRCLE('',#6926,0.505);
#730=CIRCLE('',#6928,0.7);
#731=CIRCLE('',#6929,0.7);
#964=CYLINDRICAL_SURFACE('',#6924,0.505);
#965=CYLINDRICAL_SURFACE('',#6927,0.7);
#1159=FACE_OUTER_BOUND('',#1568,.T.);
#1160=FACE_OUTER_BOUND('',#1569,.T.);
#1161=FACE_OUTER_BOUND('',#1570,.T.);
#1162=FACE_OUTER_BOUND('',#1572,.T.);
#1568=EDGE_LOOP('',(#4698,#4699,#4700,#4701));
#1569=EDGE_LOOP('',(#4702,#4703,#4704,#4705));
#1570=EDGE_LOOP('',(#4706));
#1571=EDGE_LOOP('',(#4707));
#1572=EDGE_LOOP('',(#4708));
#1573=EDGE_LOOP('',(#4709));
#2133=LINE('',#10120,#2600);
#2134=LINE('',#10126,#2601);
#2600=VECTOR('',#8124,0.505);
#2601=VECTOR('',#8131,0.7);
#3022=VERTEX_POINT('',#10117);
#3023=VERTEX_POINT('',#10119);
#3024=VERTEX_POINT('',#10123);
#3025=VERTEX_POINT('',#10125);
#3635=EDGE_CURVE('',#3022,#3022,#728,.T.);
#3636=EDGE_CURVE('',#3022,#3023,#2133,.T.);
#3637=EDGE_CURVE('',#3023,#3023,#729,.T.);
#3638=EDGE_CURVE('',#3024,#3024,#730,.T.);
#3639=EDGE_CURVE('',#3024,#3025,#2134,.T.);
#3640=EDGE_CURVE('',#3025,#3025,#731,.T.);
#4698=ORIENTED_EDGE('',*,*,#3635,.F.);
#4699=ORIENTED_EDGE('',*,*,#3636,.T.);
#4700=ORIENTED_EDGE('',*,*,#3637,.T.);
#4701=ORIENTED_EDGE('',*,*,#3636,.F.);
#4702=ORIENTED_EDGE('',*,*,#3638,.F.);
#4703=ORIENTED_EDGE('',*,*,#3639,.T.);
#4704=ORIENTED_EDGE('',*,*,#3640,.T.);
#4705=ORIENTED_EDGE('',*,*,#3639,.F.);
#4706=ORIENTED_EDGE('',*,*,#3638,.T.);
#4707=ORIENTED_EDGE('',*,*,#3635,.T.);
#4708=ORIENTED_EDGE('',*,*,#3640,.F.);
#4709=ORIENTED_EDGE('',*,*,#3637,.F.);
#5698=PLANE('',#6930);
#5699=PLANE('',#6931);
#5959=ADVANCED_FACE('',(#1159),#964,.F.);
#5960=ADVANCED_FACE('',(#1160),#965,.T.);
#5961=ADVANCED_FACE('',(#1161,#603),#5698,.T.);
#5962=ADVANCED_FACE('',(#1162,#604),#5699,.F.);
#6215=CLOSED_SHELL('',(#5959,#5960,#5961,#5962));
#6923=AXIS2_PLACEMENT_3D('',#10115,#8118,#8119);
#6924=AXIS2_PLACEMENT_3D('',#10116,#8120,#8121);
#6925=AXIS2_PLACEMENT_3D('',#10118,#8122,#8123);
#6926=AXIS2_PLACEMENT_3D('',#10121,#8125,#8126);
#6927=AXIS2_PLACEMENT_3D('',#10122,#8127,#8128);
#6928=AXIS2_PLACEMENT_3D('',#10124,#8129,#8130);
#6929=AXIS2_PLACEMENT_3D('',#10127,#8132,#8133);
#6930=AXIS2_PLACEMENT_3D('',#10128,#8134,#8135);
#6931=AXIS2_PLACEMENT_3D('',#10129,#8136,#8137);
#8118=DIRECTION('axis',(0.,0.,1.));
#8119=DIRECTION('refdir',(1.,0.,0.));
#8120=DIRECTION('center_axis',(0.,1.,0.));
#8121=DIRECTION('ref_axis',(1.,0.,0.));
#8122=DIRECTION('center_axis',(0.,-1.,0.));
#8123=DIRECTION('ref_axis',(1.,0.,0.));
#8124=DIRECTION('',(0.,-1.,0.));
#8125=DIRECTION('center_axis',(0.,-1.,0.));
#8126=DIRECTION('ref_axis',(1.,0.,0.));
#8127=DIRECTION('center_axis',(0.,1.,0.));
#8128=DIRECTION('ref_axis',(1.,0.,0.));
#8129=DIRECTION('center_axis',(0.,1.,0.));
#8130=DIRECTION('ref_axis',(1.,0.,0.));
#8131=DIRECTION('',(0.,-1.,0.));
#8132=DIRECTION('center_axis',(0.,1.,0.));
#8133=DIRECTION('ref_axis',(1.,0.,0.));
#8134=DIRECTION('center_axis',(0.,1.,0.));
#8135=DIRECTION('ref_axis',(1.,0.,0.));
#8136=DIRECTION('center_axis',(0.,1.,0.));
#8137=DIRECTION('ref_axis',(1.,0.,0.));
#10115=CARTESIAN_POINT('',(0.,0.,0.));
#10116=CARTESIAN_POINT('Origin',(-2.,-9.55,5.));
#10117=CARTESIAN_POINT('',(-2.505,-9.2,5.));
#10118=CARTESIAN_POINT('Origin',(-2.,-9.2,5.));
#10119=CARTESIAN_POINT('',(-2.505,-9.55,5.));
#10120=CARTESIAN_POINT('',(-2.505,-9.55,5.));
#10121=CARTESIAN_POINT('Origin',(-2.,-9.55,5.));
#10122=CARTESIAN_POINT('Origin',(-2.,-9.55,5.));
#10123=CARTESIAN_POINT('',(-2.7,-9.2,5.));
#10124=CARTESIAN_POINT('Origin',(-2.,-9.2,5.));
#10125=CARTESIAN_POINT('',(-2.7,-9.55,5.));
#10126=CARTESIAN_POINT('',(-2.7,-9.55,5.));
#10127=CARTESIAN_POINT('Origin',(-2.,-9.55,5.));
#10128=CARTESIAN_POINT('Origin',(-2.,-9.2,5.));
#10129=CARTESIAN_POINT('Origin',(-2.,-9.55,5.));
#11662=UNCERTAINTY_MEASURE_WITH_UNIT(LENGTH_MEASURE(0.001),#11749,
'DISTANCE_ACCURACY_VALUE',
'Maximum model space distance between geometric entities at asserted c
onnectivities');
#11699=UNCERTAINTY_MEASURE_WITH_UNIT(LENGTH_MEASURE(0.001),#11749,
'DISTANCE_ACCURACY_VALUE',
'Maximum model space distance between geometric entities at asserted c
onnectivities');
#11711=(
GEOMETRIC_REPRESENTATION_CONTEXT(3)
GLOBAL_UNCERTAINTY_ASSIGNED_CONTEXT((#11662))
GLOBAL_UNIT_ASSIGNED_CONTEXT((#11749,#11751,#11752))
REPRESENTATION_CONTEXT('','3D')
);
#11748=(
GEOMETRIC_REPRESENTATION_CONTEXT(3)
GLOBAL_UNCERTAINTY_ASSIGNED_CONTEXT((#11699))
GLOBAL_UNIT_ASSIGNED_CONTEXT((#11749,#11751,#11752))
REPRESENTATION_CONTEXT('','3D')
);
#11749=(
LENGTH_UNIT()
NAMED_UNIT(*)
SI_UNIT(.CENTI.,.METRE.)
);
#11751=(
NAMED_UNIT(*)
PLANE_ANGLE_UNIT()
SI_UNIT($,.RADIAN.)
);
#11752=(
NAMED_UNIT(*)
SI_UNIT($,.STERADIAN.)
SOLID_ANGLE_UNIT()
);
#11764=SHAPE_DEFINITION_REPRESENTATION(#11812,#11935);
#11812=PRODUCT_DEFINITION_SHAPE('',$,#11984);
#11935=SHAPE_REPRESENTATION('',(#6923),#11711);
#11972=PRODUCT_DEFINITION_CONTEXT('part definition',#12118,'design');
#11984=PRODUCT_DEFINITION('Inner race spacer_1','Inner race spacer (1)',
#12032,#11972);
#12032=PRODUCT_DEFINITION_FORMATION('',$,#12131);
#12118=APPLICATION_CONTEXT(
'Core Data for Automotive Mechanical Design Process');
#12119=PRODUCT_CONTEXT('part definition',#12118,'mechanical');
#12131=PRODUCT('Inner race spacer_1','Inner race spacer (1)',
'Inner race spacer',(#12119));
#12170=PRESENTATION_STYLE_ASSIGNMENT((#12175));
#12175=SURFACE_STYLE_USAGE(.BOTH.,#12180);
#12180=SURFACE_SIDE_STYLE('',(#12185));
#12185=SURFACE_STYLE_FILL_AREA(#12190);
#12190=FILL_AREA_STYLE('CAD Library Painted - Steel gray',(#12195));
#12195=FILL_AREA_STYLE_COLOUR('CAD Library Painted - Steel gray',#12200);
#12200=COLOUR_RGB('CAD Library Painted - Steel gray',0.592156862745098,
0.631372549019608,0.67843137254902);
ENDSEC;
END-ISO-10303-21;
